ISO-10303-21;
HEADER;
/* Generated by software containing ST-Developer
 * from STEP Tools, Inc. (www.steptools.com) 
 */

FILE_DESCRIPTION(
/* description */ ('Independent manual two-gate roller-track escapement for nominal30mm d
iameter20mm wide feed rollers. Opposed gates are driven by native capt
ured pin-slot loops with positive curved-slot travel stops at\X\B116de
g. Repeated gate/pin/washer/clip instances, adapted native common bear
ing families, full retaining lips and rotating polymer grip. External 
workpieces, gravity feeder/incline and mount anchors outside assembly.
 No powered-feed compatibility, impact, capacity, safety, force, wear 
or life rating.'),
/* implementation_level */ '2;1');

FILE_NAME(
/* name */ 'Yoke thrust washer.step',
/* time_stamp */ '2026-11-08T18:43:23-08:00',
/* author */ (''),
/* organization */ (''),
/* preprocessor_version */ 'ST-DEVELOPER v20.2',
/* originating_system */ 'Autodesk Translation Framework v15.17.0.0',
/* authorisation */ '');

FILE_SCHEMA (('AUTOMOTIVE_DESIGN { 1 0 10303 214 3 1 1 }'));
ENDSEC;

DATA;
#10=MECHANICAL_DESIGN_GEOMETRIC_PRESENTATION_REPRESENTATION('',(#461),#19863);
#423=SHAPE_REPRESENTATION_RELATIONSHIP('SRR','None',#19941,#442);
#442=ADVANCED_BREP_SHAPE_REPRESENTATION('',(#480),#19850);
#461=STYLED_ITEM('',(#20043),#480);
#480=MANIFOLD_SOLID_BREP('Body1',#6430);
#834=LINE('',#15833,#1299);
#835=LINE('',#15839,#1300);
#1299=VECTOR('',#8156,3.);
#1300=VECTOR('',#8163,5.);
#1544=CYLINDRICAL_SURFACE('',#6963,3.);
#1545=CYLINDRICAL_SURFACE('',#6966,5.);
#1665=FACE_BOUND('',#2325,.T.);
#1666=FACE_BOUND('',#2327,.T.);
#1915=FACE_OUTER_BOUND('',#2322,.T.);
#1916=FACE_OUTER_BOUND('',#2323,.T.);
#1917=FACE_OUTER_BOUND('',#2324,.T.);
#1918=FACE_OUTER_BOUND('',#2326,.T.);
#2322=EDGE_LOOP('',(#5337,#5338,#5339,#5340));
#2323=EDGE_LOOP('',(#5341,#5342,#5343,#5344));
#2324=EDGE_LOOP('',(#5345));
#2325=EDGE_LOOP('',(#5346));
#2326=EDGE_LOOP('',(#5347));
#2327=EDGE_LOOP('',(#5348));
#2554=CIRCLE('',#6964,3.);
#2555=CIRCLE('',#6965,3.);
#2556=CIRCLE('',#6967,5.);
#2557=CIRCLE('',#6968,5.);
#3024=VERTEX_POINT('',#15830);
#3025=VERTEX_POINT('',#15832);
#3026=VERTEX_POINT('',#15836);
#3027=VERTEX_POINT('',#15838);
#3827=EDGE_CURVE('',#3024,#3024,#2554,.T.);
#3828=EDGE_CURVE('',#3024,#3025,#834,.T.);
#3829=EDGE_CURVE('',#3025,#3025,#2555,.T.);
#3830=EDGE_CURVE('',#3026,#3026,#2556,.T.);
#3831=EDGE_CURVE('',#3026,#3027,#835,.T.);
#3832=EDGE_CURVE('',#3027,#3027,#2557,.T.);
#5337=ORIENTED_EDGE('',*,*,#3827,.F.);
#5338=ORIENTED_EDGE('',*,*,#3828,.T.);
#5339=ORIENTED_EDGE('',*,*,#3829,.T.);
#5340=ORIENTED_EDGE('',*,*,#3828,.F.);
#5341=ORIENTED_EDGE('',*,*,#3830,.F.);
#5342=ORIENTED_EDGE('',*,*,#3831,.T.);
#5343=ORIENTED_EDGE('',*,*,#3832,.T.);
#5344=ORIENTED_EDGE('',*,*,#3831,.F.);
#5345=ORIENTED_EDGE('',*,*,#3830,.T.);
#5346=ORIENTED_EDGE('',*,*,#3827,.T.);
#5347=ORIENTED_EDGE('',*,*,#3832,.F.);
#5348=ORIENTED_EDGE('',*,*,#3829,.F.);
#6014=PLANE('',#6969);
#6015=PLANE('',#6970);
#6294=ADVANCED_FACE('',(#1915),#1544,.F.);
#6295=ADVANCED_FACE('',(#1916),#1545,.T.);
#6296=ADVANCED_FACE('',(#1917,#1665),#6014,.T.);
#6297=ADVANCED_FACE('',(#1918,#1666),#6015,.F.);
#6430=CLOSED_SHELL('',(#6294,#6295,#6296,#6297));
#6962=AXIS2_PLACEMENT_3D('',#15828,#8150,#8151);
#6963=AXIS2_PLACEMENT_3D('',#15829,#8152,#8153);
#6964=AXIS2_PLACEMENT_3D('',#15831,#8154,#8155);
#6965=AXIS2_PLACEMENT_3D('',#15834,#8157,#8158);
#6966=AXIS2_PLACEMENT_3D('',#15835,#8159,#8160);
#6967=AXIS2_PLACEMENT_3D('',#15837,#8161,#8162);
#6968=AXIS2_PLACEMENT_3D('',#15840,#8164,#8165);
#6969=AXIS2_PLACEMENT_3D('',#15841,#8166,#8167);
#6970=AXIS2_PLACEMENT_3D('',#15842,#8168,#8169);
#8150=DIRECTION('axis',(0.,0.,1.));
#8151=DIRECTION('refdir',(1.,0.,0.));
#8152=DIRECTION('center_axis',(0.,0.,1.));
#8153=DIRECTION('ref_axis',(1.,0.,0.));
#8154=DIRECTION('center_axis',(0.,0.,-1.));
#8155=DIRECTION('ref_axis',(1.,0.,0.));
#8156=DIRECTION('',(0.,0.,-1.));
#8157=DIRECTION('center_axis',(0.,0.,-1.));
#8158=DIRECTION('ref_axis',(1.,0.,0.));
#8159=DIRECTION('center_axis',(0.,0.,1.));
#8160=DIRECTION('ref_axis',(1.,0.,0.));
#8161=DIRECTION('center_axis',(0.,0.,1.));
#8162=DIRECTION('ref_axis',(1.,0.,0.));
#8163=DIRECTION('',(0.,0.,-1.));
#8164=DIRECTION('center_axis',(0.,0.,1.));
#8165=DIRECTION('ref_axis',(1.,0.,0.));
#8166=DIRECTION('center_axis',(0.,0.,1.));
#8167=DIRECTION('ref_axis',(1.,0.,0.));
#8168=DIRECTION('center_axis',(0.,0.,1.));
#8169=DIRECTION('ref_axis',(1.,0.,0.));
#15828=CARTESIAN_POINT('',(0.,0.,0.));
#15829=CARTESIAN_POINT('Origin',(0.,0.,0.));
#15830=CARTESIAN_POINT('',(-3.,-3.67394039744206E-16,1.));
#15831=CARTESIAN_POINT('Origin',(0.,0.,1.));
#15832=CARTESIAN_POINT('',(-3.,-3.67394039744206E-16,0.));
#15833=CARTESIAN_POINT('',(-3.,-3.67394039744206E-16,0.));
#15834=CARTESIAN_POINT('Origin',(0.,0.,0.));
#15835=CARTESIAN_POINT('Origin',(0.,0.,0.));
#15836=CARTESIAN_POINT('',(-5.,-6.12323399573677E-16,1.));
#15837=CARTESIAN_POINT('Origin',(0.,0.,1.));
#15838=CARTESIAN_POINT('',(-5.,-6.12323399573677E-16,0.));
#15839=CARTESIAN_POINT('',(-5.,-6.12323399573677E-16,0.));
#15840=CARTESIAN_POINT('Origin',(0.,0.,0.));
#15841=CARTESIAN_POINT('Origin',(0.,0.,1.));
#15842=CARTESIAN_POINT('Origin',(0.,0.,0.));
#19829=UNCERTAINTY_MEASURE_WITH_UNIT(LENGTH_MEASURE(0.01),#19864,
'DISTANCE_ACCURACY_VALUE',
'Maximum model space distance between geometric entities at asserted c
onnectivities');
#19842=UNCERTAINTY_MEASURE_WITH_UNIT(LENGTH_MEASURE(0.01),#19864,
'DISTANCE_ACCURACY_VALUE',
'Maximum model space distance between geometric entities at asserted c
onnectivities');
#19850=(
GEOMETRIC_REPRESENTATION_CONTEXT(3)
GLOBAL_UNCERTAINTY_ASSIGNED_CONTEXT((#19829))
GLOBAL_UNIT_ASSIGNED_CONTEXT((#19864,#19866,#19867))
REPRESENTATION_CONTEXT('','3D')
);
#19863=(
GEOMETRIC_REPRESENTATION_CONTEXT(3)
GLOBAL_UNCERTAINTY_ASSIGNED_CONTEXT((#19842))
GLOBAL_UNIT_ASSIGNED_CONTEXT((#19864,#19866,#19867))
REPRESENTATION_CONTEXT('','3D')
);
#19864=(
LENGTH_UNIT()
NAMED_UNIT(*)
SI_UNIT(.MILLI.,.METRE.)
);
#19866=(
NAMED_UNIT(*)
PLANE_ANGLE_UNIT()
SI_UNIT($,.RADIAN.)
);
#19867=(
NAMED_UNIT(*)
SI_UNIT($,.STERADIAN.)
SOLID_ANGLE_UNIT()
);
#19875=SHAPE_DEFINITION_REPRESENTATION(#19895,#19941);
#19895=PRODUCT_DEFINITION_SHAPE('',$,#19962);
#19941=SHAPE_REPRESENTATION('',(#6962),#19850);
#19954=PRODUCT_DEFINITION_CONTEXT('part definition',#20016,'design');
#19962=PRODUCT_DEFINITION('Yoke thrust washer','Yoke thrust washer',#19982,
#19954);
#19982=PRODUCT_DEFINITION_FORMATION('',$,#20025);
#20016=APPLICATION_CONTEXT(
'Core Data for Automotive Mechanical Design Process');
#20017=PRODUCT_CONTEXT('part definition',#20016,'mechanical');
#20025=PRODUCT('Yoke thrust washer','Yoke thrust washer',$,(#20017));
#20043=PRESENTATION_STYLE_ASSIGNMENT((#20050));
#20050=SURFACE_STYLE_USAGE(.BOTH.,#20057);
#20057=SURFACE_SIDE_STYLE('',(#20064));
#20064=SURFACE_STYLE_FILL_AREA(#20071);
#20071=FILL_AREA_STYLE('Light gray',(#20078));
#20078=FILL_AREA_STYLE_COLOUR('Light gray',#20085);
#20085=COLOUR_RGB('Light gray',0.725490196078431,0.752941176470588,0.792156862745098);
ENDSEC;
END-ISO-10303-21;
